ISO-10303-21;
HEADER;
/* Generated by software containing ST-Developer
 * from STEP Tools, Inc. (www.steptools.com) 
 */

FILE_DESCRIPTION(
/* description */ ('PAT-072'),
/* implementation_level */ '2;1');

FILE_NAME(
/* name */ 'M2 sight screw (2).step',
/* time_stamp */ '2026-10-29T20:11:56-07:00',
/* author */ (''),
/* organization */ (''),
/* preprocessor_version */ 'ST-DEVELOPER v20.2',
/* originating_system */ 'Autodesk Translation Framework v15.17.0.0',
/* authorisation */ '');

FILE_SCHEMA (('AUTOMOTIVE_DESIGN { 1 0 10303 214 3 1 1 }'));
ENDSEC;

DATA;
#10=MECHANICAL_DESIGN_GEOMETRIC_PRESENTATION_REPRESENTATION('',(#356),#11432);
#284=SHAPE_REPRESENTATION_RELATIONSHIP('SRR','None',#11588,#320);
#320=ADVANCED_BREP_SHAPE_REPRESENTATION('',(#392),#11419);
#356=STYLED_ITEM('',(#11826),#392);
#392=MANIFOLD_SOLID_BREP('Body1',#6091);
#530=FACE_BOUND('',#1551,.T.);
#716=PLANE('',#6989);
#717=PLANE('',#6990);
#718=PLANE('',#6991);
#719=PLANE('',#6994);
#720=PLANE('',#6996);
#721=PLANE('',#6999);
#722=PLANE('',#7005);
#1045=FACE_OUTER_BOUND('',#1545,.T.);
#1046=FACE_OUTER_BOUND('',#1546,.T.);
#1047=FACE_OUTER_BOUND('',#1547,.T.);
#1048=FACE_OUTER_BOUND('',#1548,.T.);
#1049=FACE_OUTER_BOUND('',#1549,.T.);
#1050=FACE_OUTER_BOUND('',#1550,.T.);
#1051=FACE_OUTER_BOUND('',#1552,.T.);
#1052=FACE_OUTER_BOUND('',#1553,.T.);
#1053=FACE_OUTER_BOUND('',#1554,.T.);
#1545=EDGE_LOOP('',(#5078,#5079,#5080,#5081));
#1546=EDGE_LOOP('',(#5082,#5083,#5084,#5085));
#1547=EDGE_LOOP('',(#5086,#5087,#5088,#5089));
#1548=EDGE_LOOP('',(#5090,#5091));
#1549=EDGE_LOOP('',(#5092,#5093,#5094));
#1550=EDGE_LOOP('',(#5095));
#1551=EDGE_LOOP('',(#5096));
#1552=EDGE_LOOP('',(#5097,#5098,#5099,#5100,#5101,#5102,#5103,#5104,#5105,
#5106,#5107,#5108));
#1553=EDGE_LOOP('',(#5109,#5110,#5111,#5112));
#1554=EDGE_LOOP('',(#5113));
#1972=LINE('',#10776,#2391);
#1973=LINE('',#10778,#2392);
#1974=LINE('',#10780,#2393);
#1975=LINE('',#10781,#2394);
#1976=LINE('',#10785,#2395);
#1977=LINE('',#10787,#2396);
#1978=LINE('',#10789,#2397);
#1979=LINE('',#10790,#2398);
#1980=LINE('',#10806,#2399);
#1981=LINE('',#10810,#2400);
#2391=VECTOR('',#8499,1.);
#2392=VECTOR('',#8500,1.);
#2393=VECTOR('',#8501,1.);
#2394=VECTOR('',#8502,1.);
#2395=VECTOR('',#8505,1.);
#2396=VECTOR('',#8506,1.);
#2397=VECTOR('',#8507,1.);
#2398=VECTOR('',#8508,1.);
#2399=VECTOR('',#8533,0.175);
#2400=VECTOR('',#8538,0.1);
#2751=CIRCLE('',#6992,0.175);
#2752=CIRCLE('',#6993,0.175);
#2753=CIRCLE('',#6995,0.175);
#2754=CIRCLE('',#6997,0.175);
#2755=CIRCLE('',#6998,0.175);
#2756=CIRCLE('',#7000,0.175);
#2757=CIRCLE('',#7001,0.1);
#2758=CIRCLE('',#7004,0.1);
#3166=VERTEX_POINT('',#10774);
#3167=VERTEX_POINT('',#10775);
#3168=VERTEX_POINT('',#10777);
#3169=VERTEX_POINT('',#10779);
#3170=VERTEX_POINT('',#10783);
#3171=VERTEX_POINT('',#10784);
#3172=VERTEX_POINT('',#10786);
#3173=VERTEX_POINT('',#10788);
#3174=VERTEX_POINT('',#10797);
#3175=VERTEX_POINT('',#10801);
#3176=VERTEX_POINT('',#10803);
#3177=VERTEX_POINT('',#10808);
#3828=EDGE_CURVE('',#3166,#3167,#1972,.T.);
#3829=EDGE_CURVE('',#3166,#3168,#1973,.T.);
#3830=EDGE_CURVE('',#3169,#3168,#1974,.T.);
#3831=EDGE_CURVE('',#3167,#3169,#1975,.T.);
#3832=EDGE_CURVE('',#3170,#3171,#1976,.T.);
#3833=EDGE_CURVE('',#3172,#3170,#1977,.T.);
#3834=EDGE_CURVE('',#3173,#3172,#1978,.T.);
#3835=EDGE_CURVE('',#3173,#3171,#1979,.T.);
#3836=EDGE_CURVE('',#3171,#3166,#2751,.T.);
#3837=EDGE_CURVE('',#3168,#3173,#2752,.T.);
#3838=EDGE_CURVE('',#3172,#3170,#2753,.T.);
#3839=EDGE_CURVE('',#3174,#3169,#2754,.T.);
#3840=EDGE_CURVE('',#3167,#3174,#2755,.T.);
#3841=EDGE_CURVE('',#3175,#3175,#2756,.T.);
#3842=EDGE_CURVE('',#3176,#3176,#2757,.T.);
#3843=EDGE_CURVE('',#3175,#3174,#1980,.T.);
#3844=EDGE_CURVE('',#3177,#3177,#2758,.T.);
#3845=EDGE_CURVE('',#3177,#3176,#1981,.T.);
#5078=ORIENTED_EDGE('',*,*,#3828,.F.);
#5079=ORIENTED_EDGE('',*,*,#3829,.T.);
#5080=ORIENTED_EDGE('',*,*,#3830,.F.);
#5081=ORIENTED_EDGE('',*,*,#3831,.F.);
#5082=ORIENTED_EDGE('',*,*,#3832,.F.);
#5083=ORIENTED_EDGE('',*,*,#3833,.F.);
#5084=ORIENTED_EDGE('',*,*,#3834,.F.);
#5085=ORIENTED_EDGE('',*,*,#3835,.T.);
#5086=ORIENTED_EDGE('',*,*,#3836,.F.);
#5087=ORIENTED_EDGE('',*,*,#3835,.F.);
#5088=ORIENTED_EDGE('',*,*,#3837,.F.);
#5089=ORIENTED_EDGE('',*,*,#3829,.F.);
#5090=ORIENTED_EDGE('',*,*,#3833,.T.);
#5091=ORIENTED_EDGE('',*,*,#3838,.F.);
#5092=ORIENTED_EDGE('',*,*,#3831,.T.);
#5093=ORIENTED_EDGE('',*,*,#3839,.F.);
#5094=ORIENTED_EDGE('',*,*,#3840,.F.);
#5095=ORIENTED_EDGE('',*,*,#3841,.T.);
#5096=ORIENTED_EDGE('',*,*,#3842,.F.);
#5097=ORIENTED_EDGE('',*,*,#3841,.F.);
#5098=ORIENTED_EDGE('',*,*,#3843,.T.);
#5099=ORIENTED_EDGE('',*,*,#3839,.T.);
#5100=ORIENTED_EDGE('',*,*,#3830,.T.);
#5101=ORIENTED_EDGE('',*,*,#3837,.T.);
#5102=ORIENTED_EDGE('',*,*,#3834,.T.);
#5103=ORIENTED_EDGE('',*,*,#3838,.T.);
#5104=ORIENTED_EDGE('',*,*,#3832,.T.);
#5105=ORIENTED_EDGE('',*,*,#3836,.T.);
#5106=ORIENTED_EDGE('',*,*,#3828,.T.);
#5107=ORIENTED_EDGE('',*,*,#3840,.T.);
#5108=ORIENTED_EDGE('',*,*,#3843,.F.);
#5109=ORIENTED_EDGE('',*,*,#3844,.F.);
#5110=ORIENTED_EDGE('',*,*,#3845,.T.);
#5111=ORIENTED_EDGE('',*,*,#3842,.T.);
#5112=ORIENTED_EDGE('',*,*,#3845,.F.);
#5113=ORIENTED_EDGE('',*,*,#3844,.T.);
#5661=CYLINDRICAL_SURFACE('',#7002,0.175);
#5662=CYLINDRICAL_SURFACE('',#7003,0.1);
#5944=ADVANCED_FACE('',(#1045),#716,.F.);
#5945=ADVANCED_FACE('',(#1046),#717,.F.);
#5946=ADVANCED_FACE('',(#1047),#718,.F.);
#5947=ADVANCED_FACE('',(#1048),#719,.F.);
#5948=ADVANCED_FACE('',(#1049),#720,.F.);
#5949=ADVANCED_FACE('',(#1050,#530),#721,.T.);
#5950=ADVANCED_FACE('',(#1051),#5661,.T.);
#5951=ADVANCED_FACE('',(#1052),#5662,.T.);
#5952=ADVANCED_FACE('',(#1053),#722,.T.);
#6091=CLOSED_SHELL('',(#5944,#5945,#5946,#5947,#5948,#5949,#5950,#5951,
#5952));
#6988=AXIS2_PLACEMENT_3D('',#10772,#8495,#8496);
#6989=AXIS2_PLACEMENT_3D('',#10773,#8497,#8498);
#6990=AXIS2_PLACEMENT_3D('',#10782,#8503,#8504);
#6991=AXIS2_PLACEMENT_3D('',#10791,#8509,#8510);
#6992=AXIS2_PLACEMENT_3D('',#10792,#8511,#8512);
#6993=AXIS2_PLACEMENT_3D('',#10793,#8513,#8514);
#6994=AXIS2_PLACEMENT_3D('',#10794,#8515,#8516);
#6995=AXIS2_PLACEMENT_3D('',#10795,#8517,#8518);
#6996=AXIS2_PLACEMENT_3D('',#10796,#8519,#8520);
#6997=AXIS2_PLACEMENT_3D('',#10798,#8521,#8522);
#6998=AXIS2_PLACEMENT_3D('',#10799,#8523,#8524);
#6999=AXIS2_PLACEMENT_3D('',#10800,#8525,#8526);
#7000=AXIS2_PLACEMENT_3D('',#10802,#8527,#8528);
#7001=AXIS2_PLACEMENT_3D('',#10804,#8529,#8530);
#7002=AXIS2_PLACEMENT_3D('',#10805,#8531,#8532);
#7003=AXIS2_PLACEMENT_3D('',#10807,#8534,#8535);
#7004=AXIS2_PLACEMENT_3D('',#10809,#8536,#8537);
#7005=AXIS2_PLACEMENT_3D('',#10811,#8539,#8540);
#8495=DIRECTION('axis',(0.,0.,1.));
#8496=DIRECTION('refdir',(1.,0.,0.));
#8497=DIRECTION('center_axis',(-1.,0.,0.));
#8498=DIRECTION('ref_axis',(0.,0.,1.));
#8499=DIRECTION('',(0.,-1.,0.));
#8500=DIRECTION('',(0.,0.,1.));
#8501=DIRECTION('',(0.,1.,0.));
#8502=DIRECTION('',(0.,0.,1.));
#8503=DIRECTION('center_axis',(1.,0.,0.));
#8504=DIRECTION('ref_axis',(0.,0.,-1.));
#8505=DIRECTION('',(0.,1.,0.));
#8506=DIRECTION('',(0.,0.,-1.));
#8507=DIRECTION('',(0.,-1.,0.));
#8508=DIRECTION('',(0.,0.,-1.));
#8509=DIRECTION('center_axis',(0.,1.,0.));
#8510=DIRECTION('ref_axis',(0.,0.,1.));
#8511=DIRECTION('center_axis',(0.,1.,0.));
#8512=DIRECTION('ref_axis',(1.,0.,0.));
#8513=DIRECTION('center_axis',(0.,1.,0.));
#8514=DIRECTION('ref_axis',(1.,0.,0.));
#8515=DIRECTION('center_axis',(0.,1.,0.));
#8516=DIRECTION('ref_axis',(1.,0.,0.));
#8517=DIRECTION('center_axis',(0.,1.,0.));
#8518=DIRECTION('ref_axis',(1.,0.,0.));
#8519=DIRECTION('center_axis',(0.,1.,0.));
#8520=DIRECTION('ref_axis',(1.,0.,0.));
#8521=DIRECTION('center_axis',(0.,1.,0.));
#8522=DIRECTION('ref_axis',(1.,0.,0.));
#8523=DIRECTION('center_axis',(0.,1.,0.));
#8524=DIRECTION('ref_axis',(1.,0.,0.));
#8525=DIRECTION('center_axis',(0.,1.,0.));
#8526=DIRECTION('ref_axis',(1.,0.,0.));
#8527=DIRECTION('center_axis',(0.,1.,0.));
#8528=DIRECTION('ref_axis',(1.,0.,0.));
#8529=DIRECTION('center_axis',(0.,1.,0.));
#8530=DIRECTION('ref_axis',(1.,0.,0.));
#8531=DIRECTION('center_axis',(0.,1.,0.));
#8532=DIRECTION('ref_axis',(1.,0.,0.));
#8533=DIRECTION('',(0.,-1.,0.));
#8534=DIRECTION('center_axis',(0.,1.,0.));
#8535=DIRECTION('ref_axis',(1.,0.,0.));
#8536=DIRECTION('center_axis',(0.,1.,0.));
#8537=DIRECTION('ref_axis',(1.,0.,0.));
#8538=DIRECTION('',(0.,-1.,0.));
#8539=DIRECTION('center_axis',(0.,1.,0.));
#8540=DIRECTION('ref_axis',(1.,0.,0.));
#10772=CARTESIAN_POINT('',(0.,0.,0.));
#10773=CARTESIAN_POINT('Origin',(0.77,-3.4,9.6));
#10774=CARTESIAN_POINT('',(0.77,-3.2,9.62759060350433));
#10775=CARTESIAN_POINT('',(0.77,-3.3,9.62759060350433));
#10776=CARTESIAN_POINT('',(0.77,-3.3,9.62759060350433));
#10777=CARTESIAN_POINT('',(0.77,-3.2,9.97240939649567));
#10778=CARTESIAN_POINT('',(0.77,-3.2,10.));
#10779=CARTESIAN_POINT('',(0.77,-3.3,9.97240939649567));
#10780=CARTESIAN_POINT('',(0.77,-3.3,9.97240939649567));
#10781=CARTESIAN_POINT('',(0.77,-3.3,9.7));
#10782=CARTESIAN_POINT('Origin',(0.83,-3.4,10.));
#10783=CARTESIAN_POINT('',(0.83,-3.3,9.62759060350433));
#10784=CARTESIAN_POINT('',(0.83,-3.2,9.62759060350433));
#10785=CARTESIAN_POINT('',(0.83,-3.3,9.62759060350433));
#10786=CARTESIAN_POINT('',(0.83,-3.3,9.97240939649567));
#10787=CARTESIAN_POINT('',(0.83,-3.3,9.9));
#10788=CARTESIAN_POINT('',(0.83,-3.2,9.97240939649567));
#10789=CARTESIAN_POINT('',(0.83,-3.3,9.97240939649567));
#10790=CARTESIAN_POINT('',(0.83,-3.2,9.6));
#10791=CARTESIAN_POINT('Origin',(0.8,-3.2,9.8));
#10792=CARTESIAN_POINT('Origin',(0.8,-3.2,9.8));
#10793=CARTESIAN_POINT('Origin',(0.8,-3.2,9.8));
#10794=CARTESIAN_POINT('Origin',(0.8,-3.3,9.8));
#10795=CARTESIAN_POINT('Origin',(0.8,-3.3,9.8));
#10796=CARTESIAN_POINT('Origin',(0.8,-3.3,9.8));
#10797=CARTESIAN_POINT('',(0.625,-3.3,9.8));
#10798=CARTESIAN_POINT('Origin',(0.8,-3.3,9.8));
#10799=CARTESIAN_POINT('Origin',(0.8,-3.3,9.8));
#10800=CARTESIAN_POINT('Origin',(0.8,-3.1,9.8));
#10801=CARTESIAN_POINT('',(0.625,-3.1,9.8));
#10802=CARTESIAN_POINT('Origin',(0.8,-3.1,9.8));
#10803=CARTESIAN_POINT('',(0.7,-3.1,9.8));
#10804=CARTESIAN_POINT('Origin',(0.8,-3.1,9.8));
#10805=CARTESIAN_POINT('Origin',(0.8,-3.3,9.8));
#10806=CARTESIAN_POINT('',(0.625,-3.3,9.8));
#10807=CARTESIAN_POINT('Origin',(0.8,-3.1,9.8));
#10808=CARTESIAN_POINT('',(0.7,-2.1,9.8));
#10809=CARTESIAN_POINT('Origin',(0.8,-2.1,9.8));
#10810=CARTESIAN_POINT('',(0.7,-3.1,9.8));
#10811=CARTESIAN_POINT('Origin',(0.8,-2.1,9.8));
#11380=UNCERTAINTY_MEASURE_WITH_UNIT(LENGTH_MEASURE(0.001),#11433,
'DISTANCE_ACCURACY_VALUE',
'Maximum model space distance between geometric entities at asserted c
onnectivities');
#11393=UNCERTAINTY_MEASURE_WITH_UNIT(LENGTH_MEASURE(0.001),#11433,
'DISTANCE_ACCURACY_VALUE',
'Maximum model space distance between geometric entities at asserted c
onnectivities');
#11419=(
GEOMETRIC_REPRESENTATION_CONTEXT(3)
GLOBAL_UNCERTAINTY_ASSIGNED_CONTEXT((#11380))
GLOBAL_UNIT_ASSIGNED_CONTEXT((#11433,#11435,#11436))
REPRESENTATION_CONTEXT('','3D')
);
#11432=(
GEOMETRIC_REPRESENTATION_CONTEXT(3)
GLOBAL_UNCERTAINTY_ASSIGNED_CONTEXT((#11393))
GLOBAL_UNIT_ASSIGNED_CONTEXT((#11433,#11435,#11436))
REPRESENTATION_CONTEXT('','3D')
);
#11433=(
LENGTH_UNIT()
NAMED_UNIT(*)
SI_UNIT(.CENTI.,.METRE.)
);
#11435=(
NAMED_UNIT(*)
PLANE_ANGLE_UNIT()
SI_UNIT($,.RADIAN.)
);
#11436=(
NAMED_UNIT(*)
SI_UNIT($,.STERADIAN.)
SOLID_ANGLE_UNIT()
);
#11462=SHAPE_DEFINITION_REPRESENTATION(#11500,#11588);
#11500=PRODUCT_DEFINITION_SHAPE('',$,#11627);
#11588=SHAPE_REPRESENTATION('',(#6988),#11419);
#11601=PRODUCT_DEFINITION_CONTEXT('part definition',#11717,'design');
#11627=PRODUCT_DEFINITION('M2 sight screw (2)',
'M2 sight screw (2)',#11665,#11601);
#11665=PRODUCT_DEFINITION_FORMATION('',$,#11744);
#11717=APPLICATION_CONTEXT(
'Core Data for Automotive Mechanical Design Process');
#11718=PRODUCT_CONTEXT('part definition',#11717,'mechanical');
#11744=PRODUCT('M2 sight screw (2)','M2 sight screw (2)',
'M2 sight screw (2)',(#11718));
#11820=COLOUR_RGB('Black',0.12,0.14,0.17);
#11821=FILL_AREA_STYLE_COLOUR('',#11820);
#11822=FILL_AREA_STYLE('',(#11821));
#11823=SURFACE_STYLE_FILL_AREA(#11822);
#11824=SURFACE_SIDE_STYLE('',(#11823));
#11825=SURFACE_STYLE_USAGE(.BOTH.,#11824);
#11826=PRESENTATION_STYLE_ASSIGNMENT((#11825));
ENDSEC;
END-ISO-10303-21;
